ISO-10303-21;
HEADER;
FILE_DESCRIPTION (('STEP AP214'),
    '1' );
FILE_NAME ('Flywheel Manual Operating Handles.step',
    '2026-10-24T00:28:05',
    ( '' ),
    ( '' ),
    'SwSTEP 2.0',
    'SolidWorks 2025',
    '' );
FILE_SCHEMA (( 'AUTOMOTIVE_DESIGN' ));
ENDSEC;

DATA;
#66=VECTOR ( 'NONE', #19621, 1000.000000000000000 ) ;
#90=DIRECTION ( 'NONE',  ( 0.000000000000000000, 0.000000000000000000, -1.000000000000000000 ) ) ;
#200=DIRECTION ( 'NONE',  ( 0.000000000000000000, 0.000000000000000000, -1.000000000000000000 ) ) ;
#265=CARTESIAN_POINT ( 'NONE',  ( 158.8141120573112630, 400.5398297725602674, 5.000000000000004441 ) ) ;
#341=ORIENTED_EDGE ( 'NONE', *, *, #9677, .F. ) ;
#347=ORIENTED_EDGE ( 'NONE', *, *, #16944, .T. ) ;
#364=VERTEX_POINT ( 'NONE', #2756 ) ;
#405=ORIENTED_EDGE ( 'NONE', *, *, #4592, .T. ) ;
#458=DIRECTION ( 'NONE',  ( 0.000000000000000000, 0.000000000000000000, -1.000000000000000000 ) ) ;
#548=EDGE_LOOP ( 'NONE', ( #5390, #12592, #4680 ) ) ;
#574=LINE ( 'NONE', #265, #16749 ) ;
#586=VECTOR ( 'NONE', #7728, 1000.000000000000114 ) ;
#590=( NAMED_UNIT ( * ) SI_UNIT ( $, .STERADIAN. ) SOLID_ANGLE_UNIT ( ) );
#633=CARTESIAN_POINT ( 'NONE',  ( 147.4234352242185935, 610.7448905601785327, 1.893624729818134345 ) ) ;
#656=ORIENTED_EDGE ( 'NONE', *, *, #14084, .F. ) ;
#696=DIRECTION ( 'NONE',  ( 1.000000000000000000, 0.000000000000000000, 0.000000000000000000 ) ) ;
#750=CARTESIAN_POINT ( 'NONE',  ( 158.8141120573112630, 628.3356379279406383, 0.000000000000000000 ) ) ;
#769=ORIENTED_EDGE ( 'NONE', *, *, #17344, .T. ) ;
#808=CARTESIAN_POINT ( 'NONE',  ( 0.000000000000000000, 0.000000000000000000, 0.000000000000000000 ) ) ;
#820=ORIENTED_EDGE ( 'NONE', *, *, #20266, .T. ) ;
#845=ORIENTED_EDGE ( 'NONE', *, *, #11128, .T. ) ;
#927=ORIENTED_EDGE ( 'NONE', *, *, #15522, .T. ) ;
#1029=AXIS2_PLACEMENT_3D ( 'NONE', #12383, #12816, #15857 ) ;
#1048=EDGE_CURVE ( 'NONE', #11244, #13873, #10557, .T. ) ;
#1059=ORIENTED_EDGE ( 'NONE', *, *, #16308, .T. ) ;
#1062=EDGE_LOOP ( 'NONE', ( #17844, #2192, #17637, #9146 ) ) ;
#1064=VERTEX_POINT ( 'NONE', #7638 ) ;
#1090=VERTEX_POINT ( 'NONE', #17595 ) ;
#1182=VECTOR ( 'NONE', #7811, 1000.000000000000000 ) ;
#1192=VERTEX_POINT ( 'NONE', #18783 ) ;
#1196=VERTEX_POINT ( 'NONE', #3967 ) ;
#1257=ORIENTED_EDGE ( 'NONE', *, *, #3412, .F. ) ;
#1314=ORIENTED_EDGE ( 'NONE', *, *, #12746, .F. ) ;
#1338=VERTEX_POINT ( 'NONE', #7945 ) ;
#1362=EDGE_LOOP ( 'NONE', ( #15988, #9440, #20923, #7596 ) ) ;
#1364=DIRECTION ( 'NONE',  ( 0.000000000000000000, 0.000000000000000000, -1.000000000000000000 ) ) ;
#1470=CYLINDRICAL_SURFACE ( 'NONE', #4091, 5.000000000000004441 ) ;
#1484=DIRECTION ( 'NONE',  ( 0.000000000000000000, 0.000000000000000000, -1.000000000000000000 ) ) ;
#1503=LINE ( 'NONE', #8294, #4888 ) ;
#1653=DIRECTION ( 'NONE',  ( 0.000000000000000000, -0.000000000000000000, 1.000000000000000000 ) ) ;
#1666=PRODUCT_DEFINITION_SHAPE ( 'NONE', 'NONE',  #11071 ) ;
#1689=ORIENTED_EDGE ( 'NONE', *, *, #11921, .T. ) ;
#1764=DIRECTION ( 'NONE',  ( 0.000000000000000000, 1.000000000000000000, 0.000000000000000000 ) ) ;
#1799=ADVANCED_FACE ( 'NONE', ( #2762 ), #9339, .F. ) ;
#1844=CARTESIAN_POINT ( 'NONE',  ( 170.2047888904039610, 610.7448905601785327, -1.893624729818132124 ) ) ;
#2020=ORIENTED_EDGE ( 'NONE', *, *, #19133, .T. ) ;
#2030=DIRECTION ( 'NONE',  ( -0.000000000000000000, -1.000000000000000000, -0.000000000000000000 ) ) ;
#2031=FACE_OUTER_BOUND ( 'NONE', #11176, .T. ) ;
#2108=VECTOR ( 'NONE', #6888, 1000.000000000000000 ) ;
#2137=VERTEX_POINT ( 'NONE', #19940 ) ;
#2141=ORIENTED_EDGE ( 'NONE', *, *, #11380, .F. ) ;
#2156=CIRCLE ( 'NONE', #17007, 4.999999999999990230 ) ;
#2159=EDGE_CURVE ( 'NONE', #1196, #10794, #11347, .T. ) ;
#2178=LINE ( 'NONE', #8971, #4278 ) ;
#2192=ORIENTED_EDGE ( 'NONE', *, *, #11921, .F. ) ;
#2313=SHAPE_REPRESENTATION_RELATIONSHIP ( 'NONE' , 'NONE' ,  #3392, #17723 ) ;
#2340=AXIS2_PLACEMENT_3D ( 'NONE', #7984, #14613, #21197 ) ;
#2419=DIRECTION ( 'NONE',  ( 0.000000000000000000, 0.000000000000000000, 1.000000000000000000 ) ) ;
#2431=EDGE_LOOP ( 'NONE', ( #845, #5187, #3987, #17616, #13939 ) ) ;
#2469=DIRECTION ( 'NONE',  ( -0.000000000000000000, -1.000000000000000000, -0.000000000000000000 ) ) ;
#2566=ORIENTED_EDGE ( 'NONE', *, *, #12043, .F. ) ;
#2633=LINE ( 'NONE', #17762, #7965 ) ;
#2678=CIRCLE ( 'NONE', #14773, 10.00000000000000888 ) ;
#2693=CIRCLE ( 'NONE', #15825, 5.000000000000004441 ) ;
#2756=CARTESIAN_POINT ( 'NONE',  ( 151.4788465195079823, 620.7448905601785327, -8.917803138848077182 ) ) ;
#2757=LINE ( 'NONE', #2969, #20753 ) ;
#2762=FACE_OUTER_BOUND ( 'NONE', #12670, .T. ) ;
#2764=CARTESIAN_POINT ( 'NONE',  ( 158.8141120573112630, 620.7448905601785327, 4.999999999999990230 ) ) ;
#2778=ORIENTED_EDGE ( 'NONE', *, *, #3803, .T. ) ;
#2851=AXIS2_PLACEMENT_3D ( 'NONE', #10011, #18238, #200 ) ;
#2969=CARTESIAN_POINT ( 'NONE',  ( 162.8695233526006803, 620.7448905601785327, -10.81142786866620575 ) ) ;
#3036=VERTEX_POINT ( 'NONE', #19754 ) ;
#3088=ORIENTED_EDGE ( 'NONE', *, *, #18213, .T. ) ;
#3098=EDGE_LOOP ( 'NONE', ( #21304, #3311, #17459 ) ) ;
#3218=CARTESIAN_POINT ( 'NONE',  ( 162.8695233526006803, 620.7448905601785327, -10.81142786866620575 ) ) ;
#3246=DIRECTION ( 'NONE',  ( -0.9864615503757148129, 0.000000000000000000, 0.1639927121256942455 ) ) ;
#3285=CARTESIAN_POINT ( 'NONE',  ( 166.1493775951145437, 610.7448905601785327, 8.917803138848105604 ) ) ;
#3311=ORIENTED_EDGE ( 'NONE', *, *, #4592, .F. ) ;
#3329=EDGE_CURVE ( 'NONE', #19472, #18782, #19828, .T. ) ;
#3351=LINE ( 'NONE', #19784, #8741 ) ;
#3352=ADVANCED_FACE ( 'NONE', ( #16590 ), #8347, .F. ) ;
#3381=LINE ( 'NONE', #4885, #586 ) ;
#3392=SHAPE_REPRESENTATION ( 'Flywheel Manual Operating Handles', ( #12794 ), #16261 ) ;
#3412=EDGE_CURVE ( 'NONE', #8722, #8747, #574, .T. ) ;
#3428=LINE ( 'NONE', #10323, #5964 ) ;
#3460=EDGE_LOOP ( 'NONE', ( #1257, #820, #12694, #3088 ) ) ;
#3530=CARTESIAN_POINT ( 'NONE',  ( 157.1741849360543313, 610.7448905601785327, -9.864615503757139692 ) ) ;
#3584=CARTESIAN_POINT ( 'NONE',  ( 158.8141120573112630, 610.7448905601785327, -10.00000000000000888 ) ) ;
#3586=PRODUCT_DEFINITION_CONTEXT ( 'detailed design', #11918, 'design' ) ;
#3601=CARTESIAN_POINT ( 'NONE',  ( 0.000000000000000000, 610.7448905601785327, 0.000000000000000000 ) ) ;
#3644=CARTESIAN_POINT ( 'NONE',  ( 0.000000000000000000, 620.7448905601785327, 0.000000000000000000 ) ) ;
#3677=CARTESIAN_POINT ( 'NONE',  ( 158.8141120573112630, 610.7448905601785327, 0.000000000000000000 ) ) ;
#3734=DIRECTION ( 'NONE',  ( 0.3512089204514987073, 0.000000000000000000, -0.9362971185447986899 ) ) ;
#3747=FACE_OUTER_BOUND ( 'NONE', #10596, .T. ) ;
#3797=EDGE_CURVE ( 'NONE', #19262, #5413, #5264, .T. ) ;
#3803=EDGE_CURVE ( 'NONE', #19262, #1064, #20467, .T. ) ;
#3871=AXIS2_PLACEMENT_3D ( 'NONE', #4595, #6316, #9561 ) ;
#3893=CARTESIAN_POINT ( 'NONE',  ( 0.000000000000000000, 610.7448905601785327, 0.000000000000000000 ) ) ;
#3894=APPLICATION_CONTEXT ( 'automotive_design' ) ;
#3967=CARTESIAN_POINT ( 'NONE',  ( 166.1493775951145437, 620.7448905601785327, 8.917803138848105604 ) ) ;
#3987=ORIENTED_EDGE ( 'NONE', *, *, #13718, .F. ) ;
#4007=ORIENTED_EDGE ( 'NONE', *, *, #20720, .T. ) ;
#4016=AXIS2_PLACEMENT_3D ( 'NONE', #9698, #21174, #10998 ) ;
#4027=( LENGTH_UNIT ( ) NAMED_UNIT ( * ) SI_UNIT ( .MILLI., .METRE. ) );
#4091=AXIS2_PLACEMENT_3D ( 'NONE', #14778, #11299, #1364 ) ;
#4153=ORIENTED_EDGE ( 'NONE', *, *, #20293, .F. ) ;
#4179=VECTOR ( 'NONE', #6208, 1000.000000000000114 ) ;
#4225=MANIFOLD_SOLID_BREP ( 'Boss-Extrude22', #11056 ) ;
#4259=VERTEX_POINT ( 'NONE', #3218 ) ;
#4278=VECTOR ( 'NONE', #15277, 1000.000000000000114 ) ;
#4287=LINE ( 'NONE', #12510, #17174 ) ;
#4290=ORIENTED_EDGE ( 'NONE', *, *, #13282, .T. ) ;
#4303=DIRECTION ( 'NONE',  ( -0.000000000000000000, -1.000000000000000000, -0.000000000000000000 ) ) ;
#4384=ADVANCED_FACE ( 'NONE', ( #2031 ), #11751, .T. ) ;
#4423=ORIENTED_EDGE ( 'NONE', *, *, #2159, .F. ) ;
#4516=( NAMED_UNIT ( * ) SI_UNIT ( $, .STERADIAN. ) SOLID_ANGLE_UNIT ( ) );
#4522=EDGE_CURVE ( 'NONE', #8747, #13873, #2156, .T. ) ;
#4588=FACE_OUTER_BOUND ( 'NONE', #17325, .T. ) ;
#4592=EDGE_CURVE ( 'NONE', #2137, #18782, #10424, .T. ) ;
#4595=CARTESIAN_POINT ( 'NONE',  ( 158.8141120573112630, 610.7448905601785327, 0.000000000000000000 ) ) ;
#4609=ORIENTED_EDGE ( 'NONE', *, *, #14084, .T. ) ;
#4680=ORIENTED_EDGE ( 'NONE', *, *, #11128, .F. ) ;
#4688=EDGE_CURVE ( 'NONE', #14788, #11298, #12823, .T. ) ;
#4696=CARTESIAN_POINT ( 'NONE',  ( 147.4234352242185935, 620.7448905601785327, 1.893624729818134345 ) ) ;
#4808=ORIENTED_EDGE ( 'NONE', *, *, #20677, .T. ) ;
#4809=AXIS2_PLACEMENT_3D ( 'NONE', #15959, #8028, #17986 ) ;
#4821=DIRECTION ( 'NONE',  ( -0.000000000000000000, -1.000000000000000000, -0.000000000000000000 ) ) ;
#4830=CARTESIAN_POINT ( 'NONE',  ( 154.7587007620219026, 620.7448905601785327, 10.81142786866622885 ) ) ;
#4863=ORIENTED_EDGE ( 'NONE', *, *, #16944, .F. ) ;
#4885=CARTESIAN_POINT ( 'NONE',  ( 170.2047888904039610, 610.7448905601785327, -1.893624729818132124 ) ) ;
#4888=VECTOR ( 'NONE', #13183, 1000.000000000000114 ) ;
#4970=CARTESIAN_POINT ( 'NONE',  ( 166.1493775951145437, 620.7448905601785327, 8.917803138848105604 ) ) ;
#4974=ORIENTED_EDGE ( 'NONE', *, *, #4522, .T. ) ;
#5187=ORIENTED_EDGE ( 'NONE', *, *, #5192, .T. ) ;
#5192=EDGE_CURVE ( 'NONE', #8982, #1338, #2633, .T. ) ;
#5203=DIRECTION ( 'NONE',  ( -0.000000000000000000, -1.000000000000000000, -0.000000000000000000 ) ) ;
#5264=CIRCLE ( 'NONE', #13574, 10.00000000000000888 ) ;
#5390=ORIENTED_EDGE ( 'NONE', *, *, #8818, .F. ) ;
#5413=VERTEX_POINT ( 'NONE', #3584 ) ;
#5434=( NAMED_UNIT ( * ) PLANE_ANGLE_UNIT ( ) SI_UNIT ( $, .RADIAN. ) );
#5503=CARTESIAN_POINT ( 'NONE',  ( 170.2047888904039610, 620.7448905601785327, -1.893624729818132124 ) ) ;
#5520=PLANE ( 'NONE',  #19783 ) ;
#5626=CARTESIAN_POINT ( 'NONE',  ( 0.000000000000000000, 610.7448905601785327, 0.000000000000000000 ) ) ;
#5680=PLANE ( 'NONE',  #15592 ) ;
#5716=ORIENTED_EDGE ( 'NONE', *, *, #11380, .T. ) ;
#5725=FACE_OUTER_BOUND ( 'NONE', #3098, .T. ) ;
#5770=DIRECTION ( 'NONE',  ( -0.000000000000000000, -1.000000000000000000, -0.000000000000000000 ) ) ;
#5801=ORIENTED_EDGE ( 'NONE', *, *, #12746, .T. ) ;
#5890=DIRECTION ( 'NONE',  ( 0.000000000000000000, 0.000000000000000000, -1.000000000000000000 ) ) ;
#5898=DIRECTION ( 'NONE',  ( 0.000000000000000000, 0.000000000000000000, 1.000000000000000000 ) ) ;
#5928=ORIENTED_EDGE ( 'NONE', *, *, #17501, .T. ) ;
#5955=CARTESIAN_POINT ( 'NONE',  ( 162.8695233526006803, 610.7448905601785327, -10.81142786866620575 ) ) ;
#5964=VECTOR ( 'NONE', #10008, 1000.000000000000114 ) ;
#5974=CARTESIAN_POINT ( 'NONE',  ( 158.8141120573112630, 400.5398297725603243, 0.000000000000000000 ) ) ;
#5994=AXIS2_PLACEMENT_3D ( 'NONE', #15230, #13502, #6990 ) ;
#6081=EDGE_LOOP ( 'NONE', ( #19533, #7304 ) ) ;
#6127=LINE ( 'NONE', #12412, #11150 ) ;
#6158=ORIENTED_EDGE ( 'NONE', *, *, #3412, .T. ) ;
#6208=DIRECTION ( 'NONE',  ( 0.9864615503757148129, 0.000000000000000000, -0.1639927121256943288 ) ) ;
#6221=FACE_OUTER_BOUND ( 'NONE', #19635, .T. ) ;
#6288=DIRECTION ( 'NONE',  ( 0.000000000000000000, 0.000000000000000000, -1.000000000000000000 ) ) ;
#6300=AXIS2_PLACEMENT_3D ( 'NONE', #15753, #20829, #5890 ) ;
#6316=DIRECTION ( 'NONE',  ( -0.000000000000000000, -1.000000000000000000, -0.000000000000000000 ) ) ;
#6428=PLANE ( 'NONE',  #16609 ) ;
#6475=ORIENTED_EDGE ( 'NONE', *, *, #16308, .F. ) ;
#6559=PLANE ( 'NONE',  #7354 ) ;
#6562=CARTESIAN_POINT ( 'NONE',  ( 158.8141120573112630, 628.3356379279406383, -5.000000000000004441 ) ) ;
#6655=CYLINDRICAL_SURFACE ( 'NONE', #10262, 5.000000000000004441 ) ;
#6686=VECTOR ( 'NONE', #4303, 1000.000000000000000 ) ;
#6750=ORIENTED_EDGE ( 'NONE', *, *, #10787, .T. ) ;
#6819=CARTESIAN_POINT ( 'NONE',  ( 158.8141120573112630, 610.7448905601785327, 0.000000000000000000 ) ) ;
#6832=DIRECTION ( 'NONE',  ( -0.000000000000000000, -1.000000000000000000, -0.000000000000000000 ) ) ;
#6888=DIRECTION ( 'NONE',  ( -0.000000000000000000, -1.000000000000000000, -0.000000000000000000 ) ) ;
#6899=ADVANCED_FACE ( 'NONE', ( #16428 ), #6559, .F. ) ;
#6941=PLANE ( 'NONE',  #10389 ) ;
#6984=DIRECTION ( 'NONE',  ( 0.000000000000000000, 1.000000000000000000, 0.000000000000000000 ) ) ;
#6990=DIRECTION ( 'NONE',  ( 0.000000000000000000, -0.000000000000000000, 1.000000000000000000 ) ) ;
#7051=PRODUCT_CONTEXT ( 'NONE', #3894, 'mechanical' ) ;
#7110=DIRECTION ( 'NONE',  ( 0.000000000000000000, 0.000000000000000000, -1.000000000000000000 ) ) ;
#7186=DIRECTION ( 'NONE',  ( -0.6352526299242177155, 0.000000000000000000, -0.7723044064191041391 ) ) ;
#7219=ORIENTED_EDGE ( 'NONE', *, *, #1048, .F. ) ;
#7294=EDGE_CURVE ( 'NONE', #1196, #19472, #17773, .T. ) ;
#7297=FACE_OUTER_BOUND ( 'NONE', #2431, .T. ) ;
#7304=ORIENTED_EDGE ( 'NONE', *, *, #20266, .F. ) ;
#7315=DIRECTION ( 'NONE',  ( 0.000000000000000000, 0.000000000000000000, -1.000000000000000000 ) ) ;
#7321=VECTOR ( 'NONE', #19165, 1000.000000000000114 ) ;
#7354=AXIS2_PLACEMENT_3D ( 'NONE', #10420, #9915, #9806 ) ;
#7410=EDGE_LOOP ( 'NONE', ( #769, #14038, #12513, #19574, #1059, #14918 ) ) ;
#7428=ADVANCED_FACE ( 'NONE', ( #3747 ), #10444, .F. ) ;
#7511=LINE ( 'NONE', #9462, #4179 ) ;
#7572=DIRECTION ( 'NONE',  ( -0.000000000000000000, -1.000000000000000000, -0.000000000000000000 ) ) ;
#7596=ORIENTED_EDGE ( 'NONE', *, *, #20720, .F. ) ;
#7638=CARTESIAN_POINT ( 'NONE',  ( 151.4788465195079823, 610.7448905601785327, -8.917803138848077182 ) ) ;
#7711=ADVANCED_FACE ( 'NONE', ( #14464 ), #1470, .T. ) ;
#7728=DIRECTION ( 'NONE',  ( -0.6352526299242171604, 0.000000000000000000, -0.7723044064191046942 ) ) ;
#7737=AXIS2_PLACEMENT_3D ( 'NONE', #10286, #13878, #16906 ) ;
#7781=ORIENTED_EDGE ( 'NONE', *, *, #7294, .F. ) ;
#7811=DIRECTION ( 'NONE',  ( -0.000000000000000000, -1.000000000000000000, -0.000000000000000000 ) ) ;
#7945=CARTESIAN_POINT ( 'NONE',  ( 154.7587007620219026, 610.7448905601785327, 10.81142786866622885 ) ) ;
#7965=VECTOR ( 'NONE', #12584, 1000.000000000000114 ) ;
#7984=CARTESIAN_POINT ( 'NONE',  ( 0.000000000000000000, 610.7448905601785327, 0.000000000000000000 ) ) ;
#8028=DIRECTION ( 'NONE',  ( -0.1639927121256943288, 0.000000000000000000, -0.9864615503757149240 ) ) ;
#8064=( NAMED_UNIT ( * ) PLANE_ANGLE_UNIT ( ) SI_UNIT ( $, .RADIAN. ) );
#8294=CARTESIAN_POINT ( 'NONE',  ( 147.4234352242185935, 610.7448905601785327, 1.893624729818134345 ) ) ;
#8347=PLANE ( 'NONE',  #7737 ) ;
#8350=FACE_OUTER_BOUND ( 'NONE', #548, .T. ) ;
#8390=CIRCLE ( 'NONE', #20487, 10.00000000000000888 ) ;
#8403=ORIENTED_EDGE ( 'NONE', *, *, #19133, .F. ) ;
#8547=ADVANCED_FACE ( 'NONE', ( #18449 ), #17051, .F. ) ;
#8602=FACE_OUTER_BOUND ( 'NONE', #7410, .T. ) ;
#8648=DIRECTION ( 'NONE',  ( -0.000000000000000000, -1.000000000000000000, -0.000000000000000000 ) ) ;
#8722=VERTEX_POINT ( 'NONE', #9128 ) ;
#8738=ADVANCED_FACE ( 'NONE', ( #4588 ), #17572, .F. ) ;
#8741=VECTOR ( 'NONE', #3246, 1000.000000000000114 ) ;
#8747=VERTEX_POINT ( 'NONE', #2764 ) ;
#8753=DIRECTION ( 'NONE',  ( 0.000000000000000000, 0.000000000000000000, -1.000000000000000000 ) ) ;
#8818=EDGE_CURVE ( 'NONE', #1192, #11298, #17676, .T. ) ;
#8927=CARTESIAN_POINT ( 'NONE',  ( 158.8141120573112630, 400.5398297725602674, 9.999999999999994671 ) ) ;
#8971=CARTESIAN_POINT ( 'NONE',  ( 147.4234352242185935, 620.7448905601785327, 1.893624729818134345 ) ) ;
#8976=CARTESIAN_POINT ( 'NONE',  ( 151.4788465195079823, 610.7448905601785327, -8.917803138848077182 ) ) ;
#8982=VERTEX_POINT ( 'NONE', #10509 ) ;
#9128=CARTESIAN_POINT ( 'NONE',  ( 158.8141120573112630, 628.3356379279406383, 5.000000000000004441 ) ) ;
#9140=DIRECTION ( 'NONE',  ( -0.000000000000000000, -1.000000000000000000, -0.000000000000000000 ) ) ;
#9146=ORIENTED_EDGE ( 'NONE', *, *, #18861, .F. ) ;
#9232=CARTESIAN_POINT ( 'NONE',  ( 158.8141120573112630, 610.7448905601785327, 0.000000000000000000 ) ) ;
#9280=AXIS2_PLACEMENT_3D ( 'NONE', #13487, #20082, #3734 ) ;
#9328=EDGE_LOOP ( 'NONE', ( #16776, #927, #2141, #4423, #10880 ) ) ;
#9339=PLANE ( 'NONE',  #4809 ) ;
#9440=ORIENTED_EDGE ( 'NONE', *, *, #20677, .F. ) ;
#9462=CARTESIAN_POINT ( 'NONE',  ( 154.7587007620219026, 610.7448905601785327, 10.81142786866622885 ) ) ;
#9544=CARTESIAN_POINT ( 'NONE',  ( 166.1493775951145437, 620.7448905601785327, 8.917803138848105604 ) ) ;
#9561=DIRECTION ( 'NONE',  ( 0.000000000000000000, 0.000000000000000000, -1.000000000000000000 ) ) ;
#9586=LINE ( 'NONE', #11212, #17716 ) ;
#9677=EDGE_CURVE ( 'NONE', #1192, #19262, #17596, .T. ) ;
#9698=CARTESIAN_POINT ( 'NONE',  ( 153.8141120573112630, 628.3356379279406383, 0.000000000000000000 ) ) ;
#9806=DIRECTION ( 'NONE',  ( 0.6352526299242171604, 0.000000000000000000, 0.7723044064191046942 ) ) ;
#9915=DIRECTION ( 'NONE',  ( -0.7723044064191046942, 0.000000000000000000, 0.6352526299242171604 ) ) ;
#10008=DIRECTION ( 'NONE',  ( 0.9864615503757148129, 0.000000000000000000, -0.1639927121256943288 ) ) ;
#10011=CARTESIAN_POINT ( 'NONE',  ( 158.8141120573112630, 400.5398297725602674, 0.000000000000000000 ) ) ;
#10157=VERTEX_POINT ( 'NONE', #19561 ) ;
#10202=CARTESIAN_POINT ( 'NONE',  ( 162.8695233526006803, 610.7448905601785327, -10.81142786866620575 ) ) ;
#10218=CARTESIAN_POINT ( 'NONE',  ( 158.8141120573112630, 400.5398297725602674, 0.000000000000000000 ) ) ;
#10226=DIRECTION ( 'NONE',  ( 0.000000000000000000, -0.000000000000000000, 1.000000000000000000 ) ) ;
#10262=AXIS2_PLACEMENT_3D ( 'NONE', #10218, #4821, #1484 ) ;
#10267=ADVANCED_FACE ( 'NONE', ( #16659 ), #11560, .T. ) ;
#10285=VERTEX_POINT ( 'NONE', #1844 ) ;
#10286=CARTESIAN_POINT ( 'NONE',  ( 166.1493775951145437, 620.7448905601785327, 8.917803138848105604 ) ) ;
#10323=CARTESIAN_POINT ( 'NONE',  ( 154.7587007620219026, 610.7448905601785327, 10.81142786866622885 ) ) ;
#10389=AXIS2_PLACEMENT_3D ( 'NONE', #3601, #13451, #11606 ) ;
#10420=CARTESIAN_POINT ( 'NONE',  ( 170.2047888904039610, 620.7448905601785327, -1.893624729818132124 ) ) ;
#10424=CIRCLE ( 'NONE', #3871, 10.00000000000000888 ) ;
#10425=ORIENTED_EDGE ( 'NONE', *, *, #4688, .F. ) ;
#10444=PLANE ( 'NONE',  #5994 ) ;
#10509=CARTESIAN_POINT ( 'NONE',  ( 151.0910679931202196, 610.7448905601785327, 6.352526299242177821 ) ) ;
#10540=DIRECTION ( 'NONE',  ( 0.000000000000000000, 1.000000000000000000, 0.000000000000000000 ) ) ;
#10557=LINE ( 'NONE', #12408, #15259 ) ;
#10567=VECTOR ( 'NONE', #17918, 1000.000000000000000 ) ;
#10593=DIRECTION ( 'NONE',  ( -0.3512089204514986518, 0.000000000000000000, 0.9362971185447986899 ) ) ;
#10596=EDGE_LOOP ( 'NONE', ( #4290, #17664 ) ) ;
#10616=EDGE_CURVE ( 'NONE', #364, #14788, #19795, .T. ) ;
#10743=DIRECTION ( 'NONE',  ( 0.000000000000000000, 0.000000000000000000, -1.000000000000000000 ) ) ;
#10749=CARTESIAN_POINT ( 'NONE',  ( 151.4788465195079823, 610.7448905601785327, -8.917803138848077182 ) ) ;
#10750=AXIS2_PLACEMENT_3D ( 'NONE', #3677, #15160, #8753 ) ;
#10787=EDGE_CURVE ( 'NONE', #10157, #12627, #19053, .T. ) ;
#10794=VERTEX_POINT ( 'NONE', #5503 ) ;
#10880=ORIENTED_EDGE ( 'NONE', *, *, #7294, .T. ) ;
#10976=EDGE_LOOP ( 'NONE', ( #5928, #6158, #4974, #7219 ) ) ;
#10998=DIRECTION ( 'NONE',  ( 0.000000000000000000, 0.000000000000000000, -1.000000000000000000 ) ) ;
#11018=AXIS2_PLACEMENT_3D ( 'NONE', #13328, #8648, #458 ) ;
#11056=CLOSED_SHELL ( 'NONE', ( #4384, #14787, #13721, #7711, #18595, #20159, #16773, #8738, #12137, #18044, #17390, #6899, #11598, #8547, #12537, #1799, #3352, #7428, #10267 ) ) ;
#11071=PRODUCT_DEFINITION ( 'UNKNOWN', '', #15246, #3586 ) ;
#11101=DIRECTION ( 'NONE',  ( -0.000000000000000000, -1.000000000000000000, -0.000000000000000000 ) ) ;
#11128=EDGE_CURVE ( 'NONE', #11298, #8982, #1503, .T. ) ;
#11150=VECTOR ( 'NONE', #19433, 1000.000000000000114 ) ;
#11176=EDGE_LOOP ( 'NONE', ( #6750, #4609, #13416, #4153, #1689, #405, #347 ) ) ;
#11200=VECTOR ( 'NONE', #16485, 999.9999999999998863 ) ;
#11212=CARTESIAN_POINT ( 'NONE',  ( 151.4788465195079823, 620.7448905601785327, -8.917803138848077182 ) ) ;
#11237=FACE_OUTER_BOUND ( 'NONE', #1362, .T. ) ;
#11244=VERTEX_POINT ( 'NONE', #6562 ) ;
#11294=VECTOR ( 'NONE', #15095, 1000.000000000000114 ) ;
#11298=VERTEX_POINT ( 'NONE', #633 ) ;
#11299=DIRECTION ( 'NONE',  ( -0.000000000000000000, -1.000000000000000000, -0.000000000000000000 ) ) ;
#11347=LINE ( 'NONE', #4970, #20000 ) ;
#11366=CARTESIAN_POINT ( 'NONE',  ( 0.000000000000000000, 610.7448905601785327, 0.000000000000000000 ) ) ;
#11380=EDGE_CURVE ( 'NONE', #10794, #10285, #11659, .T. ) ;
#11446=DIRECTION ( 'NONE',  ( 0.3512089204514979301, 0.000000000000000000, -0.9362971185447991340 ) ) ;
#11560=CYLINDRICAL_SURFACE ( 'NONE', #14862, 9.999999999999994671 ) ;
#11568=DIRECTION ( 'NONE',  ( 0.3512089204514979301, 0.000000000000000000, -0.9362971185447991340 ) ) ;
#11598=ADVANCED_FACE ( 'NONE', ( #6221 ), #6428, .F. ) ;
#11606=DIRECTION ( 'NONE',  ( 0.000000000000000000, -0.000000000000000000, 1.000000000000000000 ) ) ;
#11659=LINE ( 'NONE', #15138, #2108 ) ;
#11751=CYLINDRICAL_SURFACE ( 'NONE', #2851, 9.999999999999994671 ) ;
#11754=FACE_BOUND ( 'NONE', #17947, .T. ) ;
#11761=CIRCLE ( 'NONE', #19707, 10.00000000000000888 ) ;
#11880=DIRECTION ( 'NONE',  ( 0.000000000000000000, 0.000000000000000000, -1.000000000000000000 ) ) ;
#11918=APPLICATION_CONTEXT ( 'automotive_design' ) ;
#11921=EDGE_CURVE ( 'NONE', #5413, #2137, #11761, .T. ) ;
#12020=ORIENTED_EDGE ( 'NONE', *, *, #20293, .T. ) ;
#12043=EDGE_CURVE ( 'NONE', #4259, #14411, #2757, .T. ) ;
#12137=ADVANCED_FACE ( 'NONE', ( #8350 ), #6941, .F. ) ;
#12180=AXIS2_PLACEMENT_3D ( 'NONE', #16523, #2030, #90 ) ;
#12210=UNCERTAINTY_MEASURE_WITH_UNIT (LENGTH_MEASURE( 1.000000000000000082E-05 ), #16096, 'distance_accuracy_value', 'NONE');
#12286=DIRECTION ( 'NONE',  ( 0.000000000000000000, 0.000000000000000000, 1.000000000000000000 ) ) ;
#12383=CARTESIAN_POINT ( 'NONE',  ( 0.000000000000000000, 610.7448905601785327, 0.000000000000000000 ) ) ;
#12408=CARTESIAN_POINT ( 'NONE',  ( 158.8141120573112630, 400.5398297725602674, -5.000000000000004441 ) ) ;
#12412=CARTESIAN_POINT ( 'NONE',  ( 170.2047888904039610, 610.7448905601785327, -1.893624729818132124 ) ) ;
#12508=DIRECTION ( 'NONE',  ( 0.000000000000000000, 1.000000000000000000, 0.000000000000000000 ) ) ;
#12510=CARTESIAN_POINT ( 'NONE',  ( 162.8695233526006803, 620.7448905601785327, -10.81142786866620575 ) ) ;
#12513=ORIENTED_EDGE ( 'NONE', *, *, #10616, .T. ) ;
#12516=( GEOMETRIC_REPRESENTATION_CONTEXT ( 3 ) GLOBAL_UNCERTAINTY_ASSIGNED_CONTEXT ( ( #12210 ) ) GLOBAL_UNIT_ASSIGNED_CONTEXT ( ( #16096, #8064, #4516 ) ) REPRESENTATION_CONTEXT ( 'NONE', 'WORKASPACE' ) );
#12537=ADVANCED_FACE ( 'NONE', ( #7297 ), #5680, .F. ) ;
#12584=DIRECTION ( 'NONE',  ( 0.6352526299242177155, 0.000000000000000000, 0.7723044064191041391 ) ) ;
#12585=DIRECTION ( 'NONE',  ( -0.000000000000000000, -1.000000000000000000, -0.000000000000000000 ) ) ;
#12592=ORIENTED_EDGE ( 'NONE', *, *, #19135, .F. ) ;
#12627=VERTEX_POINT ( 'NONE', #17371 ) ;
#12629=DIRECTION ( 'NONE',  ( -0.000000000000000000, -1.000000000000000000, -0.000000000000000000 ) ) ;
#12662=CARTESIAN_POINT ( 'NONE',  ( 168.1770832427592666, 610.7448905601785327, 3.512089204514978746 ) ) ;
#12670=EDGE_LOOP ( 'NONE', ( #4007, #5801, #7781, #6475, #19051 ) ) ;
#12694=ORIENTED_EDGE ( 'NONE', *, *, #1048, .T. ) ;
#12727=ORIENTED_EDGE ( 'NONE', *, *, #3797, .T. ) ;
#12746=EDGE_CURVE ( 'NONE', #10157, #19472, #7511, .T. ) ;
#12794=AXIS2_PLACEMENT_3D ( 'NONE', #808, #2419, #696 ) ;
#12816=DIRECTION ( 'NONE',  ( 0.000000000000000000, 1.000000000000000000, 0.000000000000000000 ) ) ;
#12823=LINE ( 'NONE', #4696, #66 ) ;
#12957=FACE_OUTER_BOUND ( 'NONE', #6081, .T. ) ;
#13183=DIRECTION ( 'NONE',  ( 0.6352526299242177155, 0.000000000000000000, 0.7723044064191041391 ) ) ;
#13234=ORIENTED_EDGE ( 'NONE', *, *, #20859, .F. ) ;
#13270=CIRCLE ( 'NONE', #18776, 5.000000000000004441 ) ;
#13277=CARTESIAN_POINT ( 'NONE',  ( 147.4234352242185935, 620.7448905601785327, 1.893624729818134345 ) ) ;
#13282=EDGE_CURVE ( 'NONE', #16900, #3036, #18514, .T. ) ;
#13328=CARTESIAN_POINT ( 'NONE',  ( 158.8141120573112630, 610.7448905601785327, 0.000000000000000000 ) ) ;
#13393=CARTESIAN_POINT ( 'NONE',  ( 158.8141120573112630, 620.7448905601785327, -4.999999999999990230 ) ) ;
#13416=ORIENTED_EDGE ( 'NONE', *, *, #13282, .F. ) ;
#13451=DIRECTION ( 'NONE',  ( 0.000000000000000000, 1.000000000000000000, 0.000000000000000000 ) ) ;
#13455=SHAPE_DEFINITION_REPRESENTATION ( #1666, #3392 ) ;
#13487=CARTESIAN_POINT ( 'NONE',  ( 151.4788465195079823, 620.7448905601785327, -8.917803138848077182 ) ) ;
#13502=DIRECTION ( 'NONE',  ( 0.000000000000000000, 1.000000000000000000, 0.000000000000000000 ) ) ;
#13555=STYLED_ITEM('',(#21449),#4225);
#13574=AXIS2_PLACEMENT_3D ( 'NONE', #16033, #7572, #20788 ) ;
#13653=FACE_OUTER_BOUND ( 'NONE', #14116, .T. ) ;
#13718=EDGE_CURVE ( 'NONE', #1090, #1338, #19650, .T. ) ;
#13721=ADVANCED_FACE ( 'NONE', ( #12957 ), #19546, .F. ) ;
#13873=VERTEX_POINT ( 'NONE', #13393 ) ;
#13878=DIRECTION ( 'NONE',  ( -0.9362971185447991340, 0.000000000000000000, -0.3512089204514979301 ) ) ;
#13922=CARTESIAN_POINT ( 'NONE',  ( 147.4234352242185935, 620.7448905601785327, 1.893624729818134345 ) ) ;
#13939=ORIENTED_EDGE ( 'NONE', *, *, #4688, .T. ) ;
#14038=ORIENTED_EDGE ( 'NONE', *, *, #14041, .T. ) ;
#14041=EDGE_CURVE ( 'NONE', #4259, #364, #4287, .T. ) ;
#14084=EDGE_CURVE ( 'NONE', #12627, #3036, #20300, .T. ) ;
#14116=EDGE_LOOP ( 'NONE', ( #1314, #4863, #20115 ) ) ;
#14138=CARTESIAN_POINT ( 'NONE',  ( 158.8141120573112630, 620.7448905601785327, 0.000000000000000000 ) ) ;
#14411=VERTEX_POINT ( 'NONE', #10202 ) ;
#14464=FACE_OUTER_BOUND ( 'NONE', #3460, .T. ) ;
#14477=CARTESIAN_POINT ( 'NONE',  ( 158.8141120573112630, 610.7448905601785327, 0.000000000000000000 ) ) ;
#14613=DIRECTION ( 'NONE',  ( 0.000000000000000000, 1.000000000000000000, 0.000000000000000000 ) ) ;
#14744=AXIS2_PLACEMENT_3D ( 'NONE', #3644, #6984, #10226 ) ;
#14754=VECTOR ( 'NONE', #9140, 1000.000000000000000 ) ;
#14773=AXIS2_PLACEMENT_3D ( 'NONE', #6819, #5203, #16894 ) ;
#14778=CARTESIAN_POINT ( 'NONE',  ( 158.8141120573112630, 400.5398297725602674, 0.000000000000000000 ) ) ;
#14785=CARTESIAN_POINT ( 'NONE',  ( 162.8695233526006803, 620.7448905601785327, -10.81142786866620575 ) ) ;
#14787=ADVANCED_FACE ( 'NONE', ( #16630 ), #6655, .T. ) ;
#14788=VERTEX_POINT ( 'NONE', #13277 ) ;
#14862=AXIS2_PLACEMENT_3D ( 'NONE', #16972, #16762, #11880 ) ;
#14918=ORIENTED_EDGE ( 'NONE', *, *, #2159, .T. ) ;
#14971=VECTOR ( 'NONE', #10593, 1000.000000000000227 ) ;
#15095=DIRECTION ( 'NONE',  ( 0.9864615503757148129, 0.000000000000000000, -0.1639927121256943288 ) ) ;
#15138=CARTESIAN_POINT ( 'NONE',  ( 170.2047888904039610, 620.7448905601785327, -1.893624729818132124 ) ) ;
#15160=DIRECTION ( 'NONE',  ( -0.000000000000000000, -1.000000000000000000, -0.000000000000000000 ) ) ;
#15199=CARTESIAN_POINT ( 'NONE',  ( 154.7587007620219026, 620.7448905601785327, 10.81142786866622885 ) ) ;
#15230=CARTESIAN_POINT ( 'NONE',  ( 148.8141120573112914, 400.5398297725603243, 0.000000000000000000 ) ) ;
#15246=PRODUCT_DEFINITION_FORMATION_WITH_SPECIFIED_SOURCE ( 'ANY', '', #19431, .NOT_KNOWN. ) ;
#15259=VECTOR ( 'NONE', #12629, 1000.000000000000000 ) ;
#15277=DIRECTION ( 'NONE',  ( 0.6352526299242177155, 0.000000000000000000, 0.7723044064191041391 ) ) ;
#15348=AXIS2_PLACEMENT_3D ( 'NONE', #3893, #20661, #20449 ) ;
#15465=AXIS2_PLACEMENT_3D ( 'NONE', #11366, #1764, #1653 ) ;
#15514=LINE ( 'NONE', #15199, #11294 ) ;
#15522=EDGE_CURVE ( 'NONE', #18782, #10285, #19776, .T. ) ;
#15581=ORIENTED_EDGE ( 'NONE', *, *, #19135, .T. ) ;
#15592=AXIS2_PLACEMENT_3D ( 'NONE', #13922, #20510, #7186 ) ;
#15652=CARTESIAN_POINT ( 'NONE',  ( 158.8141120573112630, 620.7448905601785327, 0.000000000000000000 ) ) ;
#15672=CARTESIAN_POINT ( 'NONE',  ( 158.8141120573112630, 400.5398297725602674, -9.999999999999994671 ) ) ;
#15753=CARTESIAN_POINT ( 'NONE',  ( 158.8141120573112630, 400.5398297725603243, 0.000000000000000000 ) ) ;
#15825=AXIS2_PLACEMENT_3D ( 'NONE', #16977, #18263, #7110 ) ;
#15857=DIRECTION ( 'NONE',  ( 0.000000000000000000, -0.000000000000000000, 1.000000000000000000 ) ) ;
#15885=LINE ( 'NONE', #15672, #6686 ) ;
#15959=CARTESIAN_POINT ( 'NONE',  ( 154.7587007620219026, 620.7448905601785327, 10.81142786866622885 ) ) ;
#15988=ORIENTED_EDGE ( 'NONE', *, *, #5192, .F. ) ;
#16032=ORIENTED_EDGE ( 'NONE', *, *, #8818, .T. ) ;
#16033=CARTESIAN_POINT ( 'NONE',  ( 158.8141120573112630, 610.7448905601785327, 0.000000000000000000 ) ) ;
#16078=EDGE_LOOP ( 'NONE', ( #656, #4808, #15581, #17221, #12727, #12020, #13234 ) ) ;
#16096=( LENGTH_UNIT ( ) NAMED_UNIT ( * ) SI_UNIT ( .MILLI., .METRE. ) );
#16123=PLANE ( 'NONE',  #2340 ) ;
#16201=DIRECTION ( 'NONE',  ( 0.000000000000000000, 0.000000000000000000, -1.000000000000000000 ) ) ;
#16258=FACE_OUTER_BOUND ( 'NONE', #1062, .T. ) ;
#16261=( GEOMETRIC_REPRESENTATION_CONTEXT ( 3 ) GLOBAL_UNCERTAINTY_ASSIGNED_CONTEXT ( ( #19595 ) ) GLOBAL_UNIT_ASSIGNED_CONTEXT ( ( #4027, #5434, #590 ) ) REPRESENTATION_CONTEXT ( 'NONE', 'WORKASPACE' ) );
#16308=EDGE_CURVE ( 'NONE', #1090, #1196, #15514, .T. ) ;
#16373=ORIENTED_EDGE ( 'NONE', *, *, #18861, .T. ) ;
#16383=DIRECTION ( 'NONE',  ( -0.000000000000000000, -1.000000000000000000, -0.000000000000000000 ) ) ;
#16407=DIRECTION ( 'NONE',  ( 0.1639927121256942733, -0.000000000000000000, 0.9864615503757149240 ) ) ;
#16428=FACE_OUTER_BOUND ( 'NONE', #20872, .T. ) ;
#16485=DIRECTION ( 'NONE',  ( 0.3512089204514979301, 0.000000000000000000, -0.9362971185447991340 ) ) ;
#16523=CARTESIAN_POINT ( 'NONE',  ( 158.8141120573112630, 610.7448905601785327, 0.000000000000000000 ) ) ;
#16564=CARTESIAN_POINT ( 'NONE',  ( 151.4788465195079823, 620.7448905601785327, -8.917803138848077182 ) ) ;
#16566=ORIENTED_EDGE ( 'NONE', *, *, #17344, .F. ) ;
#16590=FACE_OUTER_BOUND ( 'NONE', #9328, .T. ) ;
#16609=AXIS2_PLACEMENT_3D ( 'NONE', #14785, #16407, #17697 ) ;
#16630=FACE_OUTER_BOUND ( 'NONE', #10976, .T. ) ;
#16644=VECTOR ( 'NONE', #16675, 1000.000000000000227 ) ;
#16659=FACE_OUTER_BOUND ( 'NONE', #16078, .T. ) ;
#16675=DIRECTION ( 'NONE',  ( -0.3512089204514986518, 0.000000000000000000, 0.9362971185447986899 ) ) ;
#16749=VECTOR ( 'NONE', #6832, 1000.000000000000000 ) ;
#16762=DIRECTION ( 'NONE',  ( -0.000000000000000000, -1.000000000000000000, -0.000000000000000000 ) ) ;
#16773=ADVANCED_FACE ( 'NONE', ( #16258 ), #18181, .F. ) ;
#16776=ORIENTED_EDGE ( 'NONE', *, *, #3329, .T. ) ;
#16852=VECTOR ( 'NONE', #11446, 999.9999999999998863 ) ;
#16894=DIRECTION ( 'NONE',  ( 0.000000000000000000, 0.000000000000000000, -1.000000000000000000 ) ) ;
#16897=DIRECTION ( 'NONE',  ( 0.000000000000000000, 1.000000000000000000, 0.000000000000000000 ) ) ;
#16900=VERTEX_POINT ( 'NONE', #20452 ) ;
#16906=DIRECTION ( 'NONE',  ( -0.3512089204514979301, 0.000000000000000000, 0.9362971185447991340 ) ) ;
#16944=EDGE_CURVE ( 'NONE', #18782, #10157, #2678, .T. ) ;
#16953=DIRECTION ( 'NONE',  ( -0.9864615503757148129, 0.000000000000000000, 0.1639927121256942455 ) ) ;
#16972=CARTESIAN_POINT ( 'NONE',  ( 158.8141120573112630, 400.5398297725602674, 0.000000000000000000 ) ) ;
#16977=CARTESIAN_POINT ( 'NONE',  ( 158.8141120573112630, 628.3356379279406383, 0.000000000000000000 ) ) ;
#17007=AXIS2_PLACEMENT_3D ( 'NONE', #15652, #10540, #12286 ) ;
#17019=CIRCLE ( 'NONE', #6300, 9.999999999999980460 ) ;
#17051=PLANE ( 'NONE',  #9280 ) ;
#17165=AXIS2_PLACEMENT_3D ( 'NONE', #14138, #12508, #5898 ) ;
#17174=VECTOR ( 'NONE', #16953, 1000.000000000000114 ) ;
#17221=ORIENTED_EDGE ( 'NONE', *, *, #9677, .T. ) ;
#17274=ORIENTED_EDGE ( 'NONE', *, *, #10616, .F. ) ;
#17276=EDGE_LOOP ( 'NONE', ( #18714, #16032, #10425, #17274, #2020 ) ) ;
#17325=EDGE_LOOP ( 'NONE', ( #19822, #341, #19185 ) ) ;
#17344=EDGE_CURVE ( 'NONE', #10794, #4259, #17939, .T. ) ;
#17367=CARTESIAN_POINT ( 'NONE',  ( 166.1493775951145437, 610.7448905601785327, 8.917803138848105604 ) ) ;
#17371=CARTESIAN_POINT ( 'NONE',  ( 158.8141120573112630, 610.7448905601785327, 10.00000000000000888 ) ) ;
#17390=ADVANCED_FACE ( 'NONE', ( #11237 ), #16123, .F. ) ;
#17459=ORIENTED_EDGE ( 'NONE', *, *, #19055, .F. ) ;
#17501=EDGE_CURVE ( 'NONE', #11244, #8722, #2693, .T. ) ;
#17510=ORIENTED_EDGE ( 'NONE', *, *, #14041, .F. ) ;
#17567=ORIENTED_EDGE ( 'NONE', *, *, #18391, .T. ) ;
#17572=PLANE ( 'NONE',  #1029 ) ;
#17595=CARTESIAN_POINT ( 'NONE',  ( 154.7587007620219026, 620.7448905601785327, 10.81142786866622885 ) ) ;
#17596=CIRCLE ( 'NONE', #11018, 10.00000000000000888 ) ;
#17616=ORIENTED_EDGE ( 'NONE', *, *, #20066, .F. ) ;
#17637=ORIENTED_EDGE ( 'NONE', *, *, #3797, .F. ) ;
#17664=ORIENTED_EDGE ( 'NONE', *, *, #20859, .T. ) ;
#17676=LINE ( 'NONE', #10749, #20343 ) ;
#17697=DIRECTION ( 'NONE',  ( 0.9864615503757148129, 0.000000000000000000, -0.1639927121256942455 ) ) ;
#17716=VECTOR ( 'NONE', #11101, 1000.000000000000000 ) ;
#17723=ADVANCED_BREP_SHAPE_REPRESENTATION ( '', ( #4225, #12794 ), #16261 ) ;
#17762=CARTESIAN_POINT ( 'NONE',  ( 147.4234352242185935, 610.7448905601785327, 1.893624729818134345 ) ) ;
#17773=LINE ( 'NONE', #9544, #1182 ) ;
#17809=DIRECTION ( 'NONE',  ( -0.000000000000000000, -1.000000000000000000, -0.000000000000000000 ) ) ;
#17835=DIRECTION ( 'NONE',  ( -0.6352526299242171604, 0.000000000000000000, -0.7723044064191046942 ) ) ;
#17844=ORIENTED_EDGE ( 'NONE', *, *, #18391, .F. ) ;
#17918=DIRECTION ( 'NONE',  ( -0.000000000000000000, -1.000000000000000000, -0.000000000000000000 ) ) ;
#17939=LINE ( 'NONE', #21087, #20642 ) ;
#17947=EDGE_LOOP ( 'NONE', ( #18828, #19286 ) ) ;
#17986=DIRECTION ( 'NONE',  ( -0.9864615503757148129, 0.000000000000000000, 0.1639927121256943010 ) ) ;
#18044=ADVANCED_FACE ( 'NONE', ( #8602, #11754 ), #18455, .T. ) ;
#18181=PLANE ( 'NONE',  #15465 ) ;
#18213=EDGE_CURVE ( 'NONE', #13873, #8747, #20613, .T. ) ;
#18238=DIRECTION ( 'NONE',  ( -0.000000000000000000, -1.000000000000000000, -0.000000000000000000 ) ) ;
#18263=DIRECTION ( 'NONE',  ( -0.000000000000000000, -1.000000000000000000, -0.000000000000000000 ) ) ;
#18391=EDGE_CURVE ( 'NONE', #2137, #14411, #3381, .T. ) ;
#18449=FACE_OUTER_BOUND ( 'NONE', #17276, .T. ) ;
#18455=PLANE ( 'NONE',  #14744 ) ;
#18514=CIRCLE ( 'NONE', #19909, 9.999999999999980460 ) ;
#18595=ADVANCED_FACE ( 'NONE', ( #13653 ), #5520, .F. ) ;
#18607=EDGE_CURVE ( 'NONE', #1064, #1192, #20030, .T. ) ;
#18711=DIRECTION ( 'NONE',  ( 0.000000000000000000, -0.000000000000000000, 1.000000000000000000 ) ) ;
#18714=ORIENTED_EDGE ( 'NONE', *, *, #18607, .T. ) ;
#18715=MECHANICAL_DESIGN_GEOMETRIC_PRESENTATION_REPRESENTATION('',(#13555),#12516);
#18776=AXIS2_PLACEMENT_3D ( 'NONE', #750, #2469, #7315 ) ;
#18782=VERTEX_POINT ( 'NONE', #12662 ) ;
#18783=CARTESIAN_POINT ( 'NONE',  ( 149.4511408718632879, 610.7448905601785327, -3.512089204514984520 ) ) ;
#18828=ORIENTED_EDGE ( 'NONE', *, *, #18213, .F. ) ;
#18861=EDGE_CURVE ( 'NONE', #14411, #19262, #3351, .T. ) ;
#19051=ORIENTED_EDGE ( 'NONE', *, *, #13718, .T. ) ;
#19053=CIRCLE ( 'NONE', #10750, 10.00000000000000888 ) ;
#19055=EDGE_CURVE ( 'NONE', #10285, #2137, #6127, .T. ) ;
#19098=CIRCLE ( 'NONE', #12180, 10.00000000000000888 ) ;
#19133=EDGE_CURVE ( 'NONE', #364, #1064, #9586, .T. ) ;
#19135=EDGE_CURVE ( 'NONE', #8982, #1192, #8390, .T. ) ;
#19165=DIRECTION ( 'NONE',  ( -0.9864615503757148129, 0.000000000000000000, 0.1639927121256942455 ) ) ;
#19185=ORIENTED_EDGE ( 'NONE', *, *, #18607, .F. ) ;
#19262=VERTEX_POINT ( 'NONE', #3530 ) ;
#19286=ORIENTED_EDGE ( 'NONE', *, *, #4522, .F. ) ;
#19301=DIRECTION ( 'NONE',  ( -0.3512089204514986518, 0.000000000000000000, 0.9362971185447986899 ) ) ;
#19352=CARTESIAN_POINT ( 'NONE',  ( 166.1493775951145437, 610.7448905601785327, 8.917803138848105604 ) ) ;
#19431=PRODUCT ( 'Flywheel Manual Operating Handles', 'Flywheel Manual Operating Handles', '', ( #7051 ) ) ;
#19433=DIRECTION ( 'NONE',  ( -0.6352526299242171604, 0.000000000000000000, -0.7723044064191046942 ) ) ;
#19472=VERTEX_POINT ( 'NONE', #17367 ) ;
#19533=ORIENTED_EDGE ( 'NONE', *, *, #17501, .F. ) ;
#19546=PLANE ( 'NONE',  #4016 ) ;
#19561=CARTESIAN_POINT ( 'NONE',  ( 160.4540391785681948, 610.7448905601785327, 9.864615503757169890 ) ) ;
#19574=ORIENTED_EDGE ( 'NONE', *, *, #20066, .T. ) ;
#19595=UNCERTAINTY_MEASURE_WITH_UNIT (LENGTH_MEASURE( 1.000000000000000082E-05 ), #4027, 'distance_accuracy_value', 'NONE');
#19621=DIRECTION ( 'NONE',  ( -0.000000000000000000, -1.000000000000000000, -0.000000000000000000 ) ) ;
#19635=EDGE_LOOP ( 'NONE', ( #16373, #2778, #8403, #17510, #20304 ) ) ;
#19650=LINE ( 'NONE', #4830, #10567 ) ;
#19707=AXIS2_PLACEMENT_3D ( 'NONE', #9232, #5770, #10743 ) ;
#19754=CARTESIAN_POINT ( 'NONE',  ( 158.8141120573112630, 400.5398297725603243, 9.999999999999980460 ) ) ;
#19776=LINE ( 'NONE', #19352, #16852 ) ;
#19783=AXIS2_PLACEMENT_3D ( 'NONE', #5626, #16897, #18711 ) ;
#19784=CARTESIAN_POINT ( 'NONE',  ( 162.8695233526006803, 610.7448905601785327, -10.81142786866620575 ) ) ;
#19795=LINE ( 'NONE', #16564, #16644 ) ;
#19822=ORIENTED_EDGE ( 'NONE', *, *, #3803, .F. ) ;
#19828=LINE ( 'NONE', #3285, #11200 ) ;
#19909=AXIS2_PLACEMENT_3D ( 'NONE', #5974, #12585, #6288 ) ;
#19940=CARTESIAN_POINT ( 'NONE',  ( 166.5371561215023348, 610.7448905601785327, -6.352526299242174268 ) ) ;
#20000=VECTOR ( 'NONE', #11568, 999.9999999999998863 ) ;
#20030=LINE ( 'NONE', #8976, #14971 ) ;
#20066=EDGE_CURVE ( 'NONE', #14788, #1090, #2178, .T. ) ;
#20082=DIRECTION ( 'NONE',  ( 0.9362971185447988010, -0.000000000000000000, 0.3512089204514987628 ) ) ;
#20115=ORIENTED_EDGE ( 'NONE', *, *, #3329, .F. ) ;
#20159=ADVANCED_FACE ( 'NONE', ( #5725 ), #20341, .F. ) ;
#20266=EDGE_CURVE ( 'NONE', #8722, #11244, #13270, .T. ) ;
#20293=EDGE_CURVE ( 'NONE', #5413, #16900, #15885, .T. ) ;
#20300=LINE ( 'NONE', #8927, #14754 ) ;
#20304=ORIENTED_EDGE ( 'NONE', *, *, #12043, .T. ) ;
#20341=PLANE ( 'NONE',  #15348 ) ;
#20343=VECTOR ( 'NONE', #19301, 1000.000000000000227 ) ;
#20449=DIRECTION ( 'NONE',  ( 0.000000000000000000, -0.000000000000000000, 1.000000000000000000 ) ) ;
#20452=CARTESIAN_POINT ( 'NONE',  ( 158.8141120573112630, 400.5398297725603243, -9.999999999999980460 ) ) ;
#20467=LINE ( 'NONE', #5955, #7321 ) ;
#20487=AXIS2_PLACEMENT_3D ( 'NONE', #14477, #17809, #16201 ) ;
#20510=DIRECTION ( 'NONE',  ( 0.7723044064191042501, 0.000000000000000000, -0.6352526299242178265 ) ) ;
#20593=ORIENTED_EDGE ( 'NONE', *, *, #19055, .T. ) ;
#20613=CIRCLE ( 'NONE', #17165, 4.999999999999990230 ) ;
#20642=VECTOR ( 'NONE', #17835, 1000.000000000000114 ) ;
#20661=DIRECTION ( 'NONE',  ( 0.000000000000000000, 1.000000000000000000, 0.000000000000000000 ) ) ;
#20677=EDGE_CURVE ( 'NONE', #12627, #8982, #19098, .T. ) ;
#20720=EDGE_CURVE ( 'NONE', #1338, #10157, #3428, .T. ) ;
#20753=VECTOR ( 'NONE', #16383, 1000.000000000000000 ) ;
#20788=DIRECTION ( 'NONE',  ( 0.000000000000000000, 0.000000000000000000, -1.000000000000000000 ) ) ;
#20829=DIRECTION ( 'NONE',  ( -0.000000000000000000, -1.000000000000000000, -0.000000000000000000 ) ) ;
#20859=EDGE_CURVE ( 'NONE', #3036, #16900, #17019, .T. ) ;
#20872=EDGE_LOOP ( 'NONE', ( #20593, #17567, #2566, #16566, #5716 ) ) ;
#20923=ORIENTED_EDGE ( 'NONE', *, *, #10787, .F. ) ;
#21087=CARTESIAN_POINT ( 'NONE',  ( 170.2047888904039610, 620.7448905601785327, -1.893624729818132124 ) ) ;
#21174=DIRECTION ( 'NONE',  ( 0.000000000000000000, -1.000000000000000000, -0.000000000000000000 ) ) ;
#21197=DIRECTION ( 'NONE',  ( 0.000000000000000000, -0.000000000000000000, 1.000000000000000000 ) ) ;
#21304=ORIENTED_EDGE ( 'NONE', *, *, #15522, .F. ) ;
#21443=COLOUR_RGB('Off White',0.89,0.88,0.83);
#21444=FILL_AREA_STYLE_COLOUR('',#21443);
#21445=FILL_AREA_STYLE('',(#21444));
#21446=SURFACE_STYLE_FILL_AREA(#21445);
#21447=SURFACE_SIDE_STYLE('',(#21446));
#21448=SURFACE_STYLE_USAGE(.BOTH.,#21447);
#21449=PRESENTATION_STYLE_ASSIGNMENT((#21448));
ENDSEC;
END-ISO-10303-21;
